ISO-10303-21;
HEADER;
/* Generated by software containing ST-Developer
 * from STEP Tools, Inc. (www.steptools.com) 
 */

FILE_DESCRIPTION(
/* description */ ('Crank-driven oscillating fan base (mechanism only)'),

/* implementation_level */ '2;1');

FILE_NAME(
/* name */ 'Lower pin keeper (1).step',
/* time_stamp */ '2026-10-28T03:25:00-07:00',
/* author */ (''),
/* organization */ (''),
/* preprocessor_version */ 'ST-DEVELOPER v20.2',
/* originating_system */ 'Autodesk Translation Framework v15.17.0.0',
/* authorisation */ '');

FILE_SCHEMA (('AUTOMOTIVE_DESIGN { 1 0 10303 214 3 1 1 }'));
ENDSEC;

DATA;
#10=MECHANICAL_DESIGN_GEOMETRIC_PRESENTATION_REPRESENTATION('',(#477),#11916);
#389=SHAPE_REPRESENTATION_RELATIONSHIP('SRR','None',#12116,#429);
#429=ADVANCED_BREP_SHAPE_REPRESENTATION('',(#524),#11907);
#477=STYLED_ITEM('',(#12375),#524);
#524=MANIFOLD_SOLID_BREP('Body1',#6108);
#677=FACE_BOUND('',#1718,.T.);
#678=FACE_BOUND('',#1720,.T.);
#843=PLANE('',#7238);
#844=PLANE('',#7239);
#1193=FACE_OUTER_BOUND('',#1715,.T.);
#1194=FACE_OUTER_BOUND('',#1716,.T.);
#1195=FACE_OUTER_BOUND('',#1717,.T.);
#1196=FACE_OUTER_BOUND('',#1719,.T.);
#1715=EDGE_LOOP('',(#5292,#5293,#5294,#5295));
#1716=EDGE_LOOP('',(#5296,#5297,#5298,#5299));
#1717=EDGE_LOOP('',(#5300));
#1718=EDGE_LOOP('',(#5301));
#1719=EDGE_LOOP('',(#5302));
#1720=EDGE_LOOP('',(#5303));
#2046=LINE('',#11481,#2379);
#2047=LINE('',#11487,#2380);
#2379=VECTOR('',#9009,0.225);
#2380=VECTOR('',#9016,0.6);
#2787=CIRCLE('',#7233,0.225);
#2788=CIRCLE('',#7234,0.225);
#2789=CIRCLE('',#7236,0.6);
#2790=CIRCLE('',#7237,0.6);
#3247=VERTEX_POINT('',#11478);
#3248=VERTEX_POINT('',#11480);
#3249=VERTEX_POINT('',#11484);
#3250=VERTEX_POINT('',#11486);
#3941=EDGE_CURVE('',#3247,#3247,#2787,.T.);
#3942=EDGE_CURVE('',#3247,#3248,#2046,.T.);
#3943=EDGE_CURVE('',#3248,#3248,#2788,.T.);
#3944=EDGE_CURVE('',#3249,#3249,#2789,.T.);
#3945=EDGE_CURVE('',#3249,#3250,#2047,.T.);
#3946=EDGE_CURVE('',#3250,#3250,#2790,.T.);
#5292=ORIENTED_EDGE('',*,*,#3941,.F.);
#5293=ORIENTED_EDGE('',*,*,#3942,.T.);
#5294=ORIENTED_EDGE('',*,*,#3943,.T.);
#5295=ORIENTED_EDGE('',*,*,#3942,.F.);
#5296=ORIENTED_EDGE('',*,*,#3944,.F.);
#5297=ORIENTED_EDGE('',*,*,#3945,.T.);
#5298=ORIENTED_EDGE('',*,*,#3946,.T.);
#5299=ORIENTED_EDGE('',*,*,#3945,.F.);
#5300=ORIENTED_EDGE('',*,*,#3944,.T.);
#5301=ORIENTED_EDGE('',*,*,#3941,.T.);
#5302=ORIENTED_EDGE('',*,*,#3946,.F.);
#5303=ORIENTED_EDGE('',*,*,#3943,.F.);
#5675=CYLINDRICAL_SURFACE('',#7232,0.225);
#5676=CYLINDRICAL_SURFACE('',#7235,0.6);
#5999=ADVANCED_FACE('',(#1193),#5675,.F.);
#6000=ADVANCED_FACE('',(#1194),#5676,.T.);
#6001=ADVANCED_FACE('',(#1195,#677),#843,.T.);
#6002=ADVANCED_FACE('',(#1196,#678),#844,.F.);
#6108=CLOSED_SHELL('',(#5999,#6000,#6001,#6002));
#7231=AXIS2_PLACEMENT_3D('',#11476,#9003,#9004);
#7232=AXIS2_PLACEMENT_3D('',#11477,#9005,#9006);
#7233=AXIS2_PLACEMENT_3D('',#11479,#9007,#9008);
#7234=AXIS2_PLACEMENT_3D('',#11482,#9010,#9011);
#7235=AXIS2_PLACEMENT_3D('',#11483,#9012,#9013);
#7236=AXIS2_PLACEMENT_3D('',#11485,#9014,#9015);
#7237=AXIS2_PLACEMENT_3D('',#11488,#9017,#9018);
#7238=AXIS2_PLACEMENT_3D('',#11489,#9019,#9020);
#7239=AXIS2_PLACEMENT_3D('',#11490,#9021,#9022);
#9003=DIRECTION('axis',(0.,0.,1.));
#9004=DIRECTION('refdir',(1.,0.,0.));
#9005=DIRECTION('center_axis',(0.,0.,1.));
#9006=DIRECTION('ref_axis',(1.,0.,0.));
#9007=DIRECTION('center_axis',(0.,0.,-1.));
#9008=DIRECTION('ref_axis',(1.,0.,0.));
#9009=DIRECTION('',(0.,0.,-1.));
#9010=DIRECTION('center_axis',(0.,0.,-1.));
#9011=DIRECTION('ref_axis',(1.,0.,0.));
#9012=DIRECTION('center_axis',(0.,0.,1.));
#9013=DIRECTION('ref_axis',(1.,0.,0.));
#9014=DIRECTION('center_axis',(0.,0.,1.));
#9015=DIRECTION('ref_axis',(1.,0.,0.));
#9016=DIRECTION('',(0.,0.,-1.));
#9017=DIRECTION('center_axis',(0.,0.,1.));
#9018=DIRECTION('ref_axis',(1.,0.,0.));
#9019=DIRECTION('center_axis',(0.,0.,1.));
#9020=DIRECTION('ref_axis',(1.,0.,0.));
#9021=DIRECTION('center_axis',(0.,0.,1.));
#9022=DIRECTION('ref_axis',(1.,0.,0.));
#11476=CARTESIAN_POINT('',(0.,0.,0.));
#11477=CARTESIAN_POINT('Origin',(8.,4.,6.));
#11478=CARTESIAN_POINT('',(7.775,4.,6.2));
#11479=CARTESIAN_POINT('Origin',(8.,4.,6.2));
#11480=CARTESIAN_POINT('',(7.775,4.,6.));
#11481=CARTESIAN_POINT('',(7.775,4.,6.));
#11482=CARTESIAN_POINT('Origin',(8.,4.,6.));
#11483=CARTESIAN_POINT('Origin',(8.,4.,6.));
#11484=CARTESIAN_POINT('',(7.4,4.,6.2));
#11485=CARTESIAN_POINT('Origin',(8.,4.,6.2));
#11486=CARTESIAN_POINT('',(7.4,4.,6.));
#11487=CARTESIAN_POINT('',(7.4,4.,6.));
#11488=CARTESIAN_POINT('Origin',(8.,4.,6.));
#11489=CARTESIAN_POINT('Origin',(8.,4.,6.2));
#11490=CARTESIAN_POINT('Origin',(8.,4.,6.));
#11860=UNCERTAINTY_MEASURE_WITH_UNIT(LENGTH_MEASURE(0.001),#11917,
'DISTANCE_ACCURACY_VALUE',
'Maximum model space distance between geometric entities at asserted c
onnectivities');
#11869=UNCERTAINTY_MEASURE_WITH_UNIT(LENGTH_MEASURE(0.001),#11917,
'DISTANCE_ACCURACY_VALUE',
'Maximum model space distance between geometric entities at asserted c
onnectivities');
#11907=(
GEOMETRIC_REPRESENTATION_CONTEXT(3)
GLOBAL_UNCERTAINTY_ASSIGNED_CONTEXT((#11860))
GLOBAL_UNIT_ASSIGNED_CONTEXT((#11917,#11919,#11920))
REPRESENTATION_CONTEXT('','3D')
);
#11916=(
GEOMETRIC_REPRESENTATION_CONTEXT(3)
GLOBAL_UNCERTAINTY_ASSIGNED_CONTEXT((#11869))
GLOBAL_UNIT_ASSIGNED_CONTEXT((#11917,#11919,#11920))
REPRESENTATION_CONTEXT('','3D')
);
#11917=(
LENGTH_UNIT()
NAMED_UNIT(*)
SI_UNIT(.CENTI.,.METRE.)
);
#11919=(
NAMED_UNIT(*)
PLANE_ANGLE_UNIT()
SI_UNIT($,.RADIAN.)
);
#11920=(
NAMED_UNIT(*)
SI_UNIT($,.STERADIAN.)
SOLID_ANGLE_UNIT()
);
#11958=SHAPE_DEFINITION_REPRESENTATION(#12009,#12116);
#12009=PRODUCT_DEFINITION_SHAPE('',$,#12163);
#12116=SHAPE_REPRESENTATION('',(#7231),#11907);
#12125=PRODUCT_DEFINITION_CONTEXT('part definition',#12265,'design');
#12163=PRODUCT_DEFINITION('Lower pin keeper (1)','Lower pin keeper (1)',#12209,
#12125);
#12209=PRODUCT_DEFINITION_FORMATION('',$,#12304);
#12265=APPLICATION_CONTEXT(
'Core Data for Automotive Mechanical Design Process');
#12266=PRODUCT_CONTEXT('part definition',#12265,'mechanical');
#12304=PRODUCT('Lower pin keeper (1)','Lower pin keeper (1)',
'Lower pin keeper (1)',(#12266));
#12369=COLOUR_RGB('Grey',0.48,0.52,0.57);
#12370=FILL_AREA_STYLE_COLOUR('',#12369);
#12371=FILL_AREA_STYLE('',(#12370));
#12372=SURFACE_STYLE_FILL_AREA(#12371);
#12373=SURFACE_SIDE_STYLE('',(#12372));
#12374=SURFACE_STYLE_USAGE(.BOTH.,#12373);
#12375=PRESENTATION_STYLE_ASSIGNMENT((#12374));
ENDSEC;
END-ISO-10303-21;
